ISO-10303-21;
HEADER;
/* Generated by software containing ST-Developer
 * from STEP Tools, Inc. (www.steptools.com) 
 */

FILE_DESCRIPTION(
/* description */ ('Rack and pinion manual slide'),
/* implementation_level */ '2;1');

FILE_NAME(
/* name */ 'Flat Washer - M5.step',
/* time_stamp */ '2026-10-28T03:22:49-07:00',
/* author */ (''),
/* organization */ (''),
/* preprocessor_version */ 'ST-DEVELOPER v20.2',
/* originating_system */ 'Autodesk Translation Framework v15.17.0.0',
/* authorisation */ '');

FILE_SCHEMA (('AUTOMOTIVE_DESIGN { 1 0 10303 214 3 1 1 }'));
ENDSEC;

DATA;
#10=MECHANICAL_DESIGN_GEOMETRIC_PRESENTATION_REPRESENTATION('',(#748),#34851);
#615=CONICAL_SURFACE('',#14699,0.275,0.785398163397449);
#656=SHAPE_REPRESENTATION_RELATIONSHIP('SRR','None',#35091,#702);
#702=ADVANCED_BREP_SHAPE_REPRESENTATION('',(#801),#34816);
#748=STYLED_ITEM('',(#35418),#801);
#801=MANIFOLD_SOLID_BREP('Body1',#13768);
#960=FACE_BOUND('',#2619,.T.);
#961=FACE_BOUND('',#2622,.T.);
#1187=PLANE('',#14704);
#1188=PLANE('',#14708);
#1750=FACE_OUTER_BOUND('',#2616,.T.);
#1751=FACE_OUTER_BOUND('',#2617,.T.);
#1752=FACE_OUTER_BOUND('',#2618,.T.);
#1753=FACE_OUTER_BOUND('',#2620,.T.);
#1754=FACE_OUTER_BOUND('',#2621,.T.);
#2616=EDGE_LOOP('',(#10290,#10291,#10292,#10293));
#2617=EDGE_LOOP('',(#10294,#10295,#10296,#10297));
#2618=EDGE_LOOP('',(#10298));
#2619=EDGE_LOOP('',(#10299));
#2620=EDGE_LOOP('',(#10300,#10301,#10302,#10303));
#2621=EDGE_LOOP('',(#10304));
#2622=EDGE_LOOP('',(#10305));
#3604=LINE('',#20575,#4895);
#3605=LINE('',#20579,#4896);
#3606=LINE('',#20586,#4897);
#4895=VECTOR('',#16748,0.275);
#4896=VECTOR('',#16753,0.265);
#4897=VECTOR('',#16762,0.5);
#5952=CIRCLE('',#14700,0.285);
#5953=CIRCLE('',#14701,0.265);
#5954=CIRCLE('',#14703,0.265);
#5955=CIRCLE('',#14705,0.5);
#5956=CIRCLE('',#14707,0.5);
#6576=VERTEX_POINT('',#20572);
#6577=VERTEX_POINT('',#20574);
#6578=VERTEX_POINT('',#20578);
#6579=VERTEX_POINT('',#20582);
#6580=VERTEX_POINT('',#20585);
#7957=EDGE_CURVE('',#6576,#6576,#5952,.T.);
#7958=EDGE_CURVE('',#6576,#6577,#3604,.T.);
#7959=EDGE_CURVE('',#6577,#6577,#5953,.T.);
#7960=EDGE_CURVE('',#6577,#6578,#3605,.T.);
#7961=EDGE_CURVE('',#6578,#6578,#5954,.T.);
#7962=EDGE_CURVE('',#6579,#6579,#5955,.T.);
#7963=EDGE_CURVE('',#6579,#6580,#3606,.T.);
#7964=EDGE_CURVE('',#6580,#6580,#5956,.T.);
#10290=ORIENTED_EDGE('',*,*,#7957,.T.);
#10291=ORIENTED_EDGE('',*,*,#7958,.T.);
#10292=ORIENTED_EDGE('',*,*,#7959,.T.);
#10293=ORIENTED_EDGE('',*,*,#7958,.F.);
#10294=ORIENTED_EDGE('',*,*,#7959,.F.);
#10295=ORIENTED_EDGE('',*,*,#7960,.T.);
#10296=ORIENTED_EDGE('',*,*,#7961,.T.);
#10297=ORIENTED_EDGE('',*,*,#7960,.F.);
#10298=ORIENTED_EDGE('',*,*,#7962,.T.);
#10299=ORIENTED_EDGE('',*,*,#7957,.F.);
#10300=ORIENTED_EDGE('',*,*,#7962,.F.);
#10301=ORIENTED_EDGE('',*,*,#7963,.T.);
#10302=ORIENTED_EDGE('',*,*,#7964,.T.);
#10303=ORIENTED_EDGE('',*,*,#7963,.F.);
#10304=ORIENTED_EDGE('',*,*,#7964,.F.);
#10305=ORIENTED_EDGE('',*,*,#7961,.F.);
#12916=CYLINDRICAL_SURFACE('',#14702,0.265);
#12917=CYLINDRICAL_SURFACE('',#14706,0.5);
#13228=ADVANCED_FACE('',(#1750),#615,.F.);
#13229=ADVANCED_FACE('',(#1751),#12916,.F.);
#13230=ADVANCED_FACE('',(#1752,#960),#1187,.T.);
#13231=ADVANCED_FACE('',(#1753),#12917,.T.);
#13232=ADVANCED_FACE('',(#1754,#961),#1188,.F.);
#13768=CLOSED_SHELL('',(#13228,#13229,#13230,#13231,#13232));
#14698=AXIS2_PLACEMENT_3D('',#20570,#16742,#16743);
#14699=AXIS2_PLACEMENT_3D('',#20571,#16744,#16745);
#14700=AXIS2_PLACEMENT_3D('',#20573,#16746,#16747);
#14701=AXIS2_PLACEMENT_3D('',#20576,#16749,#16750);
#14702=AXIS2_PLACEMENT_3D('',#20577,#16751,#16752);
#14703=AXIS2_PLACEMENT_3D('',#20580,#16754,#16755);
#14704=AXIS2_PLACEMENT_3D('',#20581,#16756,#16757);
#14705=AXIS2_PLACEMENT_3D('',#20583,#16758,#16759);
#14706=AXIS2_PLACEMENT_3D('',#20584,#16760,#16761);
#14707=AXIS2_PLACEMENT_3D('',#20587,#16763,#16764);
#14708=AXIS2_PLACEMENT_3D('',#20588,#16765,#16766);
#16742=DIRECTION('axis',(0.,0.,1.));
#16743=DIRECTION('refdir',(1.,0.,0.));
#16744=DIRECTION('center_axis',(0.,1.,0.));
#16745=DIRECTION('ref_axis',(1.,0.,0.));
#16746=DIRECTION('center_axis',(0.,1.,0.));
#16747=DIRECTION('ref_axis',(1.,0.,0.));
#16748=DIRECTION('',(0.707106781186548,-0.707106781186547,-8.65956056235494E-17));
#16749=DIRECTION('center_axis',(0.,-1.,0.));
#16750=DIRECTION('ref_axis',(1.,0.,0.));
#16751=DIRECTION('center_axis',(0.,1.,0.));
#16752=DIRECTION('ref_axis',(1.,0.,0.));
#16753=DIRECTION('',(0.,-1.,0.));
#16754=DIRECTION('center_axis',(0.,-1.,0.));
#16755=DIRECTION('ref_axis',(1.,0.,0.));
#16756=DIRECTION('center_axis',(0.,1.,0.));
#16757=DIRECTION('ref_axis',(1.,0.,0.));
#16758=DIRECTION('center_axis',(0.,1.,0.));
#16759=DIRECTION('ref_axis',(1.,0.,0.));
#16760=DIRECTION('center_axis',(0.,1.,0.));
#16761=DIRECTION('ref_axis',(1.,0.,0.));
#16762=DIRECTION('',(0.,-1.,0.));
#16763=DIRECTION('center_axis',(0.,1.,0.));
#16764=DIRECTION('ref_axis',(1.,0.,0.));
#16765=DIRECTION('center_axis',(0.,1.,0.));
#16766=DIRECTION('ref_axis',(1.,0.,0.));
#20570=CARTESIAN_POINT('',(0.,0.,0.));
#20571=CARTESIAN_POINT('Origin',(0.,0.09,0.));
#20572=CARTESIAN_POINT('',(-0.285,0.1,3.49024337756996E-17));
#20573=CARTESIAN_POINT('Origin',(0.,0.1,0.));
#20574=CARTESIAN_POINT('',(-0.265,0.08,-3.24531401774049E-17));
#20575=CARTESIAN_POINT('',(-0.275,0.09,3.36777869765522E-17));
#20576=CARTESIAN_POINT('Origin',(0.,0.08,0.));
#20577=CARTESIAN_POINT('Origin',(0.,0.,0.));
#20578=CARTESIAN_POINT('',(-0.265,0.,3.24531401774049E-17));
#20579=CARTESIAN_POINT('',(-0.265,0.,3.24531401774049E-17));
#20580=CARTESIAN_POINT('Origin',(0.,0.,0.));
#20581=CARTESIAN_POINT('Origin',(0.,0.1,0.));
#20582=CARTESIAN_POINT('',(-0.5,0.1,6.12323399573677E-17));
#20583=CARTESIAN_POINT('Origin',(0.,0.1,0.));
#20584=CARTESIAN_POINT('Origin',(0.,0.,0.));
#20585=CARTESIAN_POINT('',(-0.5,0.,6.12323399573677E-17));
#20586=CARTESIAN_POINT('',(-0.5,0.,6.12323399573677E-17));
#20587=CARTESIAN_POINT('Origin',(0.,0.,0.));
#20588=CARTESIAN_POINT('Origin',(0.,0.,0.));
#34762=UNCERTAINTY_MEASURE_WITH_UNIT(LENGTH_MEASURE(0.001),#34852,
'DISTANCE_ACCURACY_VALUE',
'Maximum model space distance between geometric entities at asserted c
onnectivities');
#34797=UNCERTAINTY_MEASURE_WITH_UNIT(LENGTH_MEASURE(0.001),#34852,
'DISTANCE_ACCURACY_VALUE',
'Maximum model space distance between geometric entities at asserted c
onnectivities');
#34816=(
GEOMETRIC_REPRESENTATION_CONTEXT(3)
GLOBAL_UNCERTAINTY_ASSIGNED_CONTEXT((#34762))
GLOBAL_UNIT_ASSIGNED_CONTEXT((#34852,#34854,#34855))
REPRESENTATION_CONTEXT('','3D')
);
#34851=(
GEOMETRIC_REPRESENTATION_CONTEXT(3)
GLOBAL_UNCERTAINTY_ASSIGNED_CONTEXT((#34797))
GLOBAL_UNIT_ASSIGNED_CONTEXT((#34852,#34854,#34855))
REPRESENTATION_CONTEXT('','3D')
);
#34852=(
LENGTH_UNIT()
NAMED_UNIT(*)
SI_UNIT(.CENTI.,.METRE.)
);
#34854=(
NAMED_UNIT(*)
PLANE_ANGLE_UNIT()
SI_UNIT($,.RADIAN.)
);
#34855=(
NAMED_UNIT(*)
SI_UNIT($,.STERADIAN.)
SOLID_ANGLE_UNIT()
);
#34874=SHAPE_DEFINITION_REPRESENTATION(#34927,#35091);
#34927=PRODUCT_DEFINITION_SHAPE('',$,#35145);
#35091=SHAPE_REPRESENTATION('',(#14698),#34816);
#35126=PRODUCT_DEFINITION_CONTEXT('part definition',#35287,'design');
#35145=PRODUCT_DEFINITION('Flat Washer - M5','Flat Washer - M5',#35198,
#35126);
#35198=PRODUCT_DEFINITION_FORMATION('',$,#35307);
#35287=APPLICATION_CONTEXT(
'Core Data for Automotive Mechanical Design Process');
#35288=PRODUCT_CONTEXT('part definition',#35287,'mechanical');
#35307=PRODUCT('Flat Washer - M5','Flat Washer - M5','Flat Washer - M5',
(#35288));
#35412=COLOUR_RGB('Black',0.12,0.14,0.17);
#35413=FILL_AREA_STYLE_COLOUR('',#35412);
#35414=FILL_AREA_STYLE('',(#35413));
#35415=SURFACE_STYLE_FILL_AREA(#35414);
#35416=SURFACE_SIDE_STYLE('',(#35415));
#35417=SURFACE_STYLE_USAGE(.BOTH.,#35416);
#35418=PRESENTATION_STYLE_ASSIGNMENT((#35417));
ENDSEC;
END-ISO-10303-21;
